ISO-10303-21;
HEADER;
/* Generated by software containing ST-Developer
 * from STEP Tools, Inc. (www.steptools.com) 
 */

FILE_DESCRIPTION(
/* description */ ('V-block with clamp strap'),
/* implementation_level */ '2;1');

FILE_NAME(
/* name */ 'Flat Washer - M8.step',
/* time_stamp */ '2026-10-27T10:50:53-07:00',
/* author */ (''),
/* organization */ (''),
/* preprocessor_version */ 'ST-DEVELOPER v20.2',
/* originating_system */ 'Autodesk Translation Framework v15.17.0.0',
/* authorisation */ '');

FILE_SCHEMA (('AUTOMOTIVE_DESIGN { 1 0 10303 214 3 1 1 }'));
ENDSEC;

DATA;
#10=MECHANICAL_DESIGN_GEOMETRIC_PRESENTATION_REPRESENTATION('',(#284),#7344);
#242=SHAPE_REPRESENTATION_RELATIONSHIP('SRR','None',#7461,#263);
#263=ADVANCED_BREP_SHAPE_REPRESENTATION('',(#302),#7340);
#284=STYLED_ITEM('',(#7638),#302);
#302=MANIFOLD_SOLID_BREP('Body1',#4169);
#372=FACE_BOUND('',#1094,.T.);
#373=FACE_BOUND('',#1096,.T.);
#495=CIRCLE('',#4795,0.42);
#496=CIRCLE('',#4796,0.42);
#497=CIRCLE('',#4798,0.8);
#498=CIRCLE('',#4799,0.8);
#558=CYLINDRICAL_SURFACE('',#4794,0.42);
#559=CYLINDRICAL_SURFACE('',#4797,0.8);
#784=FACE_OUTER_BOUND('',#1091,.T.);
#785=FACE_OUTER_BOUND('',#1092,.T.);
#786=FACE_OUTER_BOUND('',#1093,.T.);
#787=FACE_OUTER_BOUND('',#1095,.T.);
#1091=EDGE_LOOP('',(#3672,#3673,#3674,#3675));
#1092=EDGE_LOOP('',(#3676,#3677,#3678,#3679));
#1093=EDGE_LOOP('',(#3680));
#1094=EDGE_LOOP('',(#3681));
#1095=EDGE_LOOP('',(#3682));
#1096=EDGE_LOOP('',(#3683));
#1466=LINE('',#7178,#1831);
#1467=LINE('',#7184,#1832);
#1831=VECTOR('',#5980,0.42);
#1832=VECTOR('',#5987,0.8);
#2152=VERTEX_POINT('',#7175);
#2153=VERTEX_POINT('',#7177);
#2154=VERTEX_POINT('',#7181);
#2155=VERTEX_POINT('',#7183);
#2662=EDGE_CURVE('',#2152,#2152,#495,.T.);
#2663=EDGE_CURVE('',#2152,#2153,#1466,.T.);
#2664=EDGE_CURVE('',#2153,#2153,#496,.T.);
#2665=EDGE_CURVE('',#2154,#2154,#497,.T.);
#2666=EDGE_CURVE('',#2154,#2155,#1467,.T.);
#2667=EDGE_CURVE('',#2155,#2155,#498,.T.);
#3672=ORIENTED_EDGE('',*,*,#2662,.F.);
#3673=ORIENTED_EDGE('',*,*,#2663,.T.);
#3674=ORIENTED_EDGE('',*,*,#2664,.T.);
#3675=ORIENTED_EDGE('',*,*,#2663,.F.);
#3676=ORIENTED_EDGE('',*,*,#2665,.F.);
#3677=ORIENTED_EDGE('',*,*,#2666,.T.);
#3678=ORIENTED_EDGE('',*,*,#2667,.T.);
#3679=ORIENTED_EDGE('',*,*,#2666,.F.);
#3680=ORIENTED_EDGE('',*,*,#2665,.T.);
#3681=ORIENTED_EDGE('',*,*,#2662,.T.);
#3682=ORIENTED_EDGE('',*,*,#2667,.F.);
#3683=ORIENTED_EDGE('',*,*,#2664,.F.);
#3896=PLANE('',#4800);
#3897=PLANE('',#4801);
#4130=ADVANCED_FACE('',(#784),#558,.F.);
#4131=ADVANCED_FACE('',(#785),#559,.T.);
#4132=ADVANCED_FACE('',(#786,#372),#3896,.T.);
#4133=ADVANCED_FACE('',(#787,#373),#3897,.F.);
#4169=CLOSED_SHELL('',(#4130,#4131,#4132,#4133));
#4793=AXIS2_PLACEMENT_3D('',#7173,#5974,#5975);
#4794=AXIS2_PLACEMENT_3D('',#7174,#5976,#5977);
#4795=AXIS2_PLACEMENT_3D('',#7176,#5978,#5979);
#4796=AXIS2_PLACEMENT_3D('',#7179,#5981,#5982);
#4797=AXIS2_PLACEMENT_3D('',#7180,#5983,#5984);
#4798=AXIS2_PLACEMENT_3D('',#7182,#5985,#5986);
#4799=AXIS2_PLACEMENT_3D('',#7185,#5988,#5989);
#4800=AXIS2_PLACEMENT_3D('',#7186,#5990,#5991);
#4801=AXIS2_PLACEMENT_3D('',#7187,#5992,#5993);
#5974=DIRECTION('axis',(0.,0.,1.));
#5975=DIRECTION('refdir',(1.,0.,0.));
#5976=DIRECTION('center_axis',(0.,1.,0.));
#5977=DIRECTION('ref_axis',(1.,0.,0.));
#5978=DIRECTION('center_axis',(0.,-1.,0.));
#5979=DIRECTION('ref_axis',(1.,0.,0.));
#5980=DIRECTION('',(0.,-1.,0.));
#5981=DIRECTION('center_axis',(0.,-1.,0.));
#5982=DIRECTION('ref_axis',(1.,0.,0.));
#5983=DIRECTION('center_axis',(0.,1.,0.));
#5984=DIRECTION('ref_axis',(1.,0.,0.));
#5985=DIRECTION('center_axis',(0.,1.,0.));
#5986=DIRECTION('ref_axis',(1.,0.,0.));
#5987=DIRECTION('',(0.,-1.,0.));
#5988=DIRECTION('center_axis',(0.,1.,0.));
#5989=DIRECTION('ref_axis',(1.,0.,0.));
#5990=DIRECTION('center_axis',(0.,1.,0.));
#5991=DIRECTION('ref_axis',(1.,0.,0.));
#5992=DIRECTION('center_axis',(0.,1.,0.));
#5993=DIRECTION('ref_axis',(1.,0.,0.));
#7173=CARTESIAN_POINT('',(0.,0.,0.));
#7174=CARTESIAN_POINT('Origin',(0.,0.,0.));
#7175=CARTESIAN_POINT('',(-0.42,0.16,5.14351655641888E-17));
#7176=CARTESIAN_POINT('Origin',(0.,0.16,0.));
#7177=CARTESIAN_POINT('',(-0.42,0.,5.14351655641888E-17));
#7178=CARTESIAN_POINT('',(-0.42,0.,5.14351655641888E-17));
#7179=CARTESIAN_POINT('Origin',(0.,0.,0.));
#7180=CARTESIAN_POINT('Origin',(0.,0.,0.));
#7181=CARTESIAN_POINT('',(-0.8,0.16,9.79717439317883E-17));
#7182=CARTESIAN_POINT('Origin',(0.,0.16,0.));
#7183=CARTESIAN_POINT('',(-0.8,0.,9.79717439317883E-17));
#7184=CARTESIAN_POINT('',(-0.8,0.,9.79717439317883E-17));
#7185=CARTESIAN_POINT('Origin',(0.,0.,0.));
#7186=CARTESIAN_POINT('Origin',(0.,0.16,0.));
#7187=CARTESIAN_POINT('Origin',(0.,0.,0.));
#7314=UNCERTAINTY_MEASURE_WITH_UNIT(LENGTH_MEASURE(0.001),#7345,
'DISTANCE_ACCURACY_VALUE',
'Maximum model space distance between geometric entities at asserted c
onnectivities');
#7318=UNCERTAINTY_MEASURE_WITH_UNIT(LENGTH_MEASURE(0.001),#7345,
'DISTANCE_ACCURACY_VALUE',
'Maximum model space distance between geometric entities at asserted c
onnectivities');
#7340=(
GEOMETRIC_REPRESENTATION_CONTEXT(3)
GLOBAL_UNCERTAINTY_ASSIGNED_CONTEXT((#7314))
GLOBAL_UNIT_ASSIGNED_CONTEXT((#7345,#7347,#7348))
REPRESENTATION_CONTEXT('','3D')
);
#7344=(
GEOMETRIC_REPRESENTATION_CONTEXT(3)
GLOBAL_UNCERTAINTY_ASSIGNED_CONTEXT((#7318))
GLOBAL_UNIT_ASSIGNED_CONTEXT((#7345,#7347,#7348))
REPRESENTATION_CONTEXT('','3D')
);
#7345=(
LENGTH_UNIT()
NAMED_UNIT(*)
SI_UNIT(.CENTI.,.METRE.)
);
#7347=(
NAMED_UNIT(*)
PLANE_ANGLE_UNIT()
SI_UNIT($,.RADIAN.)
);
#7348=(
NAMED_UNIT(*)
SI_UNIT($,.STERADIAN.)
SOLID_ANGLE_UNIT()
);
#7370=SHAPE_DEFINITION_REPRESENTATION(#7418,#7461);
#7418=PRODUCT_DEFINITION_SHAPE('',$,#7487);
#7461=SHAPE_REPRESENTATION('',(#4793),#7340);
#7465=PRODUCT_DEFINITION_CONTEXT('part definition',#7542,'design');
#7487=PRODUCT_DEFINITION('Flat Washer - M8','Flat Washer - M8',#7512,#7465);
#7512=PRODUCT_DEFINITION_FORMATION('',$,#7565);
#7542=APPLICATION_CONTEXT(
'Core Data for Automotive Mechanical Design Process');
#7543=PRODUCT_CONTEXT('part definition',#7542,'mechanical');
#7565=PRODUCT('Flat Washer - M8','Flat Washer - M8','Flat Washer - M8',
(#7543));
#7632=COLOUR_RGB('Black',0.12,0.14,0.17);
#7633=FILL_AREA_STYLE_COLOUR('',#7632);
#7634=FILL_AREA_STYLE('',(#7633));
#7635=SURFACE_STYLE_FILL_AREA(#7634);
#7636=SURFACE_SIDE_STYLE('',(#7635));
#7637=SURFACE_STYLE_USAGE(.BOTH.,#7636);
#7638=PRESENTATION_STYLE_ASSIGNMENT((#7637));
ENDSEC;
END-ISO-10303-21;
